ISO-10303-21;
HEADER;
/* Generated by software containing ST-Developer
 * from STEP Tools, Inc. (www.steptools.com) 
 */

FILE_DESCRIPTION(
/* description */ ('PAT-072'),
/* implementation_level */ '2;1');

FILE_NAME(
/* name */ 'Outlet tube (3).step',
/* time_stamp */ '2026-10-29T20:11:56-07:00',
/* author */ (''),
/* organization */ (''),
/* preprocessor_version */ 'ST-DEVELOPER v20.2',
/* originating_system */ 'Autodesk Translation Framework v15.17.0.0',
/* authorisation */ '');

FILE_SCHEMA (('AUTOMOTIVE_DESIGN { 1 0 10303 214 3 1 1 }'));
ENDSEC;

DATA;
#10=MECHANICAL_DESIGN_GEOMETRIC_PRESENTATION_REPRESENTATION('',(#345),#11432);
#273=SHAPE_REPRESENTATION_RELATIONSHIP('SRR','None',#11577,#309);
#309=ADVANCED_BREP_SHAPE_REPRESENTATION('',(#381),#11408);
#345=STYLED_ITEM('',(#11812),#381);
#381=MANIFOLD_SOLID_BREP('Body1',#6080);
#478=FACE_BOUND('',#1389,.T.);
#479=FACE_BOUND('',#1391,.T.);
#645=PLANE('',#6795);
#646=PLANE('',#6796);
#938=FACE_OUTER_BOUND('',#1386,.T.);
#939=FACE_OUTER_BOUND('',#1387,.T.);
#940=FACE_OUTER_BOUND('',#1388,.T.);
#941=FACE_OUTER_BOUND('',#1390,.T.);
#1386=EDGE_LOOP('',(#4624,#4625,#4626,#4627));
#1387=EDGE_LOOP('',(#4628,#4629,#4630,#4631));
#1388=EDGE_LOOP('',(#4632));
#1389=EDGE_LOOP('',(#4633));
#1390=EDGE_LOOP('',(#4634));
#1391=EDGE_LOOP('',(#4635));
#1831=LINE('',#10152,#2250);
#1832=LINE('',#10158,#2251);
#2250=VECTOR('',#7960,0.2);
#2251=VECTOR('',#7967,0.3);
#2669=CIRCLE('',#6790,0.2);
#2670=CIRCLE('',#6791,0.2);
#2671=CIRCLE('',#6793,0.3);
#2672=CIRCLE('',#6794,0.3);
#3018=VERTEX_POINT('',#10149);
#3019=VERTEX_POINT('',#10151);
#3020=VERTEX_POINT('',#10155);
#3021=VERTEX_POINT('',#10157);
#3601=EDGE_CURVE('',#3018,#3018,#2669,.T.);
#3602=EDGE_CURVE('',#3018,#3019,#1831,.T.);
#3603=EDGE_CURVE('',#3019,#3019,#2670,.T.);
#3604=EDGE_CURVE('',#3020,#3020,#2671,.T.);
#3605=EDGE_CURVE('',#3020,#3021,#1832,.T.);
#3606=EDGE_CURVE('',#3021,#3021,#2672,.T.);
#4624=ORIENTED_EDGE('',*,*,#3601,.F.);
#4625=ORIENTED_EDGE('',*,*,#3602,.T.);
#4626=ORIENTED_EDGE('',*,*,#3603,.T.);
#4627=ORIENTED_EDGE('',*,*,#3602,.F.);
#4628=ORIENTED_EDGE('',*,*,#3604,.F.);
#4629=ORIENTED_EDGE('',*,*,#3605,.T.);
#4630=ORIENTED_EDGE('',*,*,#3606,.T.);
#4631=ORIENTED_EDGE('',*,*,#3605,.F.);
#4632=ORIENTED_EDGE('',*,*,#3604,.T.);
#4633=ORIENTED_EDGE('',*,*,#3601,.T.);
#4634=ORIENTED_EDGE('',*,*,#3606,.F.);
#4635=ORIENTED_EDGE('',*,*,#3603,.F.);
#5625=CYLINDRICAL_SURFACE('',#6789,0.2);
#5626=CYLINDRICAL_SURFACE('',#6792,0.3);
#5837=ADVANCED_FACE('',(#938),#5625,.F.);
#5838=ADVANCED_FACE('',(#939),#5626,.T.);
#5839=ADVANCED_FACE('',(#940,#478),#645,.T.);
#5840=ADVANCED_FACE('',(#941,#479),#646,.F.);
#6080=CLOSED_SHELL('',(#5837,#5838,#5839,#5840));
#6788=AXIS2_PLACEMENT_3D('',#10147,#7954,#7955);
#6789=AXIS2_PLACEMENT_3D('',#10148,#7956,#7957);
#6790=AXIS2_PLACEMENT_3D('',#10150,#7958,#7959);
#6791=AXIS2_PLACEMENT_3D('',#10153,#7961,#7962);
#6792=AXIS2_PLACEMENT_3D('',#10154,#7963,#7964);
#6793=AXIS2_PLACEMENT_3D('',#10156,#7965,#7966);
#6794=AXIS2_PLACEMENT_3D('',#10159,#7968,#7969);
#6795=AXIS2_PLACEMENT_3D('',#10160,#7970,#7971);
#6796=AXIS2_PLACEMENT_3D('',#10161,#7972,#7973);
#7954=DIRECTION('axis',(0.,0.,1.));
#7955=DIRECTION('refdir',(1.,0.,0.));
#7956=DIRECTION('center_axis',(0.,1.,0.));
#7957=DIRECTION('ref_axis',(1.,0.,0.));
#7958=DIRECTION('center_axis',(0.,-1.,0.));
#7959=DIRECTION('ref_axis',(1.,0.,0.));
#7960=DIRECTION('',(0.,-1.,0.));
#7961=DIRECTION('center_axis',(0.,-1.,0.));
#7962=DIRECTION('ref_axis',(1.,0.,0.));
#7963=DIRECTION('center_axis',(0.,1.,0.));
#7964=DIRECTION('ref_axis',(1.,0.,0.));
#7965=DIRECTION('center_axis',(0.,1.,0.));
#7966=DIRECTION('ref_axis',(1.,0.,0.));
#7967=DIRECTION('',(0.,-1.,0.));
#7968=DIRECTION('center_axis',(0.,1.,0.));
#7969=DIRECTION('ref_axis',(1.,0.,0.));
#7970=DIRECTION('center_axis',(0.,1.,0.));
#7971=DIRECTION('ref_axis',(1.,0.,0.));
#7972=DIRECTION('center_axis',(0.,1.,0.));
#7973=DIRECTION('ref_axis',(1.,0.,0.));
#10147=CARTESIAN_POINT('',(0.,0.,0.));
#10148=CARTESIAN_POINT('Origin',(3.75,-6.5,4.));
#10149=CARTESIAN_POINT('',(3.55,-3.2,4.));
#10150=CARTESIAN_POINT('Origin',(3.75,-3.2,4.));
#10151=CARTESIAN_POINT('',(3.55,-6.5,4.));
#10152=CARTESIAN_POINT('',(3.55,-6.5,4.));
#10153=CARTESIAN_POINT('Origin',(3.75,-6.5,4.));
#10154=CARTESIAN_POINT('Origin',(3.75,-6.5,4.));
#10155=CARTESIAN_POINT('',(3.45,-3.2,4.));
#10156=CARTESIAN_POINT('Origin',(3.75,-3.2,4.));
#10157=CARTESIAN_POINT('',(3.45,-6.5,4.));
#10158=CARTESIAN_POINT('',(3.45,-6.5,4.));
#10159=CARTESIAN_POINT('Origin',(3.75,-6.5,4.));
#10160=CARTESIAN_POINT('Origin',(3.75,-3.2,4.));
#10161=CARTESIAN_POINT('Origin',(3.75,-6.5,4.));
#11369=UNCERTAINTY_MEASURE_WITH_UNIT(LENGTH_MEASURE(0.001),#11433,
'DISTANCE_ACCURACY_VALUE',
'Maximum model space distance between geometric entities at asserted c
onnectivities');
#11393=UNCERTAINTY_MEASURE_WITH_UNIT(LENGTH_MEASURE(0.001),#11433,
'DISTANCE_ACCURACY_VALUE',
'Maximum model space distance between geometric entities at asserted c
onnectivities');
#11408=(
GEOMETRIC_REPRESENTATION_CONTEXT(3)
GLOBAL_UNCERTAINTY_ASSIGNED_CONTEXT((#11369))
GLOBAL_UNIT_ASSIGNED_CONTEXT((#11433,#11435,#11436))
REPRESENTATION_CONTEXT('','3D')
);
#11432=(
GEOMETRIC_REPRESENTATION_CONTEXT(3)
GLOBAL_UNCERTAINTY_ASSIGNED_CONTEXT((#11393))
GLOBAL_UNIT_ASSIGNED_CONTEXT((#11433,#11435,#11436))
REPRESENTATION_CONTEXT('','3D')
);
#11433=(
LENGTH_UNIT()
NAMED_UNIT(*)
SI_UNIT(.CENTI.,.METRE.)
);
#11435=(
NAMED_UNIT(*)
PLANE_ANGLE_UNIT()
SI_UNIT($,.RADIAN.)
);
#11436=(
NAMED_UNIT(*)
SI_UNIT($,.STERADIAN.)
SOLID_ANGLE_UNIT()
);
#11451=SHAPE_DEFINITION_REPRESENTATION(#11489,#11577);
#11489=PRODUCT_DEFINITION_SHAPE('',$,#11616);
#11577=SHAPE_REPRESENTATION('',(#6788),#11408);
#11601=PRODUCT_DEFINITION_CONTEXT('part definition',#11717,'design');
#11616=PRODUCT_DEFINITION('Outlet tube (3)','Outlet tube (3)',#11654,
#11601);
#11654=PRODUCT_DEFINITION_FORMATION('',$,#11733);
#11717=APPLICATION_CONTEXT(
'Core Data for Automotive Mechanical Design Process');
#11718=PRODUCT_CONTEXT('part definition',#11717,'mechanical');
#11733=PRODUCT('Outlet tube (3)','Outlet tube (3)',
'Outlet tube (3)',(#11718));
#11806=COLOUR_RGB('Sky Blue',0.24,0.69,0.87);
#11807=FILL_AREA_STYLE_COLOUR('',#11806);
#11808=FILL_AREA_STYLE('',(#11807));
#11809=SURFACE_STYLE_FILL_AREA(#11808);
#11810=SURFACE_SIDE_STYLE('',(#11809));
#11811=SURFACE_STYLE_USAGE(.BOTH.,#11810);
#11812=PRESENTATION_STYLE_ASSIGNMENT((#11811));
ENDSEC;
END-ISO-10303-21;
